ISO-10303-21;
HEADER;
/* Generated by software containing ST-Developer
 * from STEP Tools, Inc. (www.steptools.com) 
 */

FILE_DESCRIPTION(
/* description */ (''),
/* implementation_level */ '2;1');

FILE_NAME(
/* name */ 'Right_Rod.step',
/* time_stamp */ '2026-10-19T01:30:23+06:00',
/* author */ (''),
/* organization */ (''),
/* preprocessor_version */ 'ST-DEVELOPER v20.2',
/* originating_system */ 'Autodesk Translation Framework v15.15.0.0',
/* authorisation */ '');

FILE_SCHEMA (('AUTOMOTIVE_DESIGN { 1 0 10303 214 3 1 1 }'));
ENDSEC;

DATA;
#10=MECHANICAL_DESIGN_GEOMETRIC_PRESENTATION_REPRESENTATION('',(#94),#10639);
#74=SHAPE_REPRESENTATION_RELATIONSHIP('SRR','None',#10684,#84);
#84=ADVANCED_BREP_SHAPE_REPRESENTATION('',(#104),#10636);
#94=STYLED_ITEM('',(#10790),#104);
#104=MANIFOLD_SOLID_BREP('Right_Rod',#5720);
#363=PLANE('',#6459);
#364=PLANE('',#6463);
#665=FACE_OUTER_BOUND('',#1089,.T.);
#666=FACE_OUTER_BOUND('',#1090,.T.);
#667=FACE_OUTER_BOUND('',#1091,.T.);
#1089=EDGE_LOOP('',(#4714));
#1090=EDGE_LOOP('',(#4715,#4716,#4717,#4718));
#1091=EDGE_LOOP('',(#4719));
#1443=LINE('',#10062,#1773);
#1773=VECTOR('',#8193,4.);
#2182=CIRCLE('',#6460,4.);
#2183=CIRCLE('',#6462,4.);
#2632=VERTEX_POINT('',#10057);
#2633=VERTEX_POINT('',#10060);
#3333=EDGE_CURVE('',#2632,#2632,#2182,.T.);
#3334=EDGE_CURVE('',#2633,#2633,#2183,.T.);
#3335=EDGE_CURVE('',#2633,#2632,#1443,.T.);
#4714=ORIENTED_EDGE('',*,*,#3333,.T.);
#4715=ORIENTED_EDGE('',*,*,#3334,.F.);
#4716=ORIENTED_EDGE('',*,*,#3335,.T.);
#4717=ORIENTED_EDGE('',*,*,#3333,.F.);
#4718=ORIENTED_EDGE('',*,*,#3335,.F.);
#4719=ORIENTED_EDGE('',*,*,#3334,.T.);
#5277=CYLINDRICAL_SURFACE('',#6461,4.);
#5608=ADVANCED_FACE('',(#665),#363,.T.);
#5609=ADVANCED_FACE('',(#666),#5277,.T.);
#5610=ADVANCED_FACE('',(#667),#364,.F.);
#5720=CLOSED_SHELL('',(#5608,#5609,#5610));
#6458=AXIS2_PLACEMENT_3D('',#10055,#8183,#8184);
#6459=AXIS2_PLACEMENT_3D('',#10056,#8185,#8186);
#6460=AXIS2_PLACEMENT_3D('',#10058,#8187,#8188);
#6461=AXIS2_PLACEMENT_3D('',#10059,#8189,#8190);
#6462=AXIS2_PLACEMENT_3D('',#10061,#8191,#8192);
#6463=AXIS2_PLACEMENT_3D('',#10063,#8194,#8195);
#8183=DIRECTION('axis',(0.,0.,1.));
#8184=DIRECTION('refdir',(1.,0.,0.));
#8185=DIRECTION('center_axis',(-1.,0.,0.));
#8186=DIRECTION('ref_axis',(0.,-1.,0.));
#8187=DIRECTION('center_axis',(-1.,0.,0.));
#8188=DIRECTION('ref_axis',(0.,-1.,0.));
#8189=DIRECTION('center_axis',(1.,0.,0.));
#8190=DIRECTION('ref_axis',(0.,-1.,0.));
#8191=DIRECTION('center_axis',(1.,0.,0.));
#8192=DIRECTION('ref_axis',(0.,-1.,0.));
#8193=DIRECTION('',(-1.,0.,0.));
#8194=DIRECTION('center_axis',(-1.,0.,0.));
#8195=DIRECTION('ref_axis',(0.,-1.,0.));
#10055=CARTESIAN_POINT('',(0.,0.,0.));
#10056=CARTESIAN_POINT('Origin',(-145.,-21.9999999999999,-1.92966607280848));
#10057=CARTESIAN_POINT('',(-145.,-17.9999999999999,-1.92966607280848));
#10058=CARTESIAN_POINT('Origin',(-145.,-21.9999999999999,-1.92966607280848));
#10059=CARTESIAN_POINT('Origin',(-125.,-21.9999999999999,-1.92966607280848));
#10060=CARTESIAN_POINT('',(145.,-17.9999999999999,-1.92966607280848));
#10061=CARTESIAN_POINT('Origin',(145.,-21.9999999999999,-1.92966607280848));
#10062=CARTESIAN_POINT('',(-125.,-17.9999999999999,-1.92966607280848));
#10063=CARTESIAN_POINT('Origin',(145.,-21.9999999999999,-1.92966607280848));
#10624=UNCERTAINTY_MEASURE_WITH_UNIT(LENGTH_MEASURE(0.01),#10640,
'DISTANCE_ACCURACY_VALUE',
'Maximum model space distance between geometric entities at asserted c
onnectivities');
#10627=UNCERTAINTY_MEASURE_WITH_UNIT(LENGTH_MEASURE(0.01),#10640,
'DISTANCE_ACCURACY_VALUE',
'Maximum model space distance between geometric entities at asserted c
onnectivities');
#10636=(
GEOMETRIC_REPRESENTATION_CONTEXT(3)
GLOBAL_UNCERTAINTY_ASSIGNED_CONTEXT((#10624))
GLOBAL_UNIT_ASSIGNED_CONTEXT((#10640,#10642,#10643))
REPRESENTATION_CONTEXT('','3D')
);
#10639=(
GEOMETRIC_REPRESENTATION_CONTEXT(3)
GLOBAL_UNCERTAINTY_ASSIGNED_CONTEXT((#10627))
GLOBAL_UNIT_ASSIGNED_CONTEXT((#10640,#10642,#10643))
REPRESENTATION_CONTEXT('','3D')
);
#10640=(
LENGTH_UNIT()
NAMED_UNIT(*)
SI_UNIT(.MILLI.,.METRE.)
);
#10642=(
NAMED_UNIT(*)
PLANE_ANGLE_UNIT()
SI_UNIT($,.RADIAN.)
);
#10643=(
NAMED_UNIT(*)
SI_UNIT($,.STERADIAN.)
SOLID_ANGLE_UNIT()
);
#10652=SHAPE_DEFINITION_REPRESENTATION(#10663,#10684);
#10663=PRODUCT_DEFINITION_SHAPE('',$,#10696);
#10684=SHAPE_REPRESENTATION('',(#6458),#10636);
#10687=PRODUCT_DEFINITION_CONTEXT('part definition',#10722,'design');
#10696=PRODUCT_DEFINITION('Right_Rod','Right_Rod',#10707,#10687);
#10707=PRODUCT_DEFINITION_FORMATION('',$,#10732);
#10722=APPLICATION_CONTEXT(
'Core Data for Automotive Mechanical Design Process');
#10723=PRODUCT_CONTEXT('part definition',#10722,'mechanical');
#10732=PRODUCT('Right_Rod','Right_Rod',$,(#10723));
#10784=COLOUR_RGB('Grey',0.48,0.52,0.57);
#10785=FILL_AREA_STYLE_COLOUR('',#10784);
#10786=FILL_AREA_STYLE('',(#10785));
#10787=SURFACE_STYLE_FILL_AREA(#10786);
#10788=SURFACE_SIDE_STYLE('',(#10787));
#10789=SURFACE_STYLE_USAGE(.BOTH.,#10788);
#10790=PRESENTATION_STYLE_ASSIGNMENT((#10789));
ENDSEC;
END-ISO-10303-21;
